ISO-10303-21;
HEADER;
/* Generated by software containing ST-Developer
 * from STEP Tools, Inc. (www.steptools.com) 
 */

FILE_DESCRIPTION(
/* description */ ('Chain-less indexing wheel (Geneva) drive'),
/* implementation_level */ '2;1');

FILE_NAME(
/* name */ 'M4x4 collar screw.step',
/* time_stamp */ '2026-10-28T03:25:22-07:00',
/* author */ (''),
/* organization */ (''),
/* preprocessor_version */ 'ST-DEVELOPER v20.2',
/* originating_system */ 'Autodesk Translation Framework v15.17.0.0',
/* authorisation */ '');

FILE_SCHEMA (('AUTOMOTIVE_DESIGN { 1 0 10303 214 3 1 1 }'));
ENDSEC;

DATA;
#10=MECHANICAL_DESIGN_GEOMETRIC_PRESENTATION_REPRESENTATION('',(#335),#10957);
#210=CONICAL_SURFACE('',#6729,0.185,0.785398163397449);
#277=SHAPE_REPRESENTATION_RELATIONSHIP('SRR','None',#11093,#302);
#302=ADVANCED_BREP_SHAPE_REPRESENTATION('',(#366),#10956);
#335=STYLED_ITEM('',(#11294),#366);
#366=MANIFOLD_SOLID_BREP('Body1',#5733);
#471=FACE_BOUND('',#1420,.T.);
#643=PLANE('',#6718);
#644=PLANE('',#6720);
#645=PLANE('',#6721);
#646=PLANE('',#6722);
#647=PLANE('',#6723);
#648=PLANE('',#6724);
#649=PLANE('',#6725);
#650=PLANE('',#6726);
#651=PLANE('',#6727);
#974=FACE_OUTER_BOUND('',#1411,.T.);
#975=FACE_OUTER_BOUND('',#1412,.T.);
#976=FACE_OUTER_BOUND('',#1413,.T.);
#977=FACE_OUTER_BOUND('',#1414,.T.);
#978=FACE_OUTER_BOUND('',#1415,.T.);
#979=FACE_OUTER_BOUND('',#1416,.T.);
#980=FACE_OUTER_BOUND('',#1417,.T.);
#981=FACE_OUTER_BOUND('',#1418,.T.);
#982=FACE_OUTER_BOUND('',#1419,.T.);
#983=FACE_OUTER_BOUND('',#1421,.T.);
#984=FACE_OUTER_BOUND('',#1422,.T.);
#1411=EDGE_LOOP('',(#5197));
#1412=EDGE_LOOP('',(#5198,#5199,#5200,#5201));
#1413=EDGE_LOOP('',(#5202,#5203,#5204,#5205));
#1414=EDGE_LOOP('',(#5206,#5207,#5208,#5209));
#1415=EDGE_LOOP('',(#5210,#5211,#5212,#5213));
#1416=EDGE_LOOP('',(#5214,#5215,#5216,#5217));
#1417=EDGE_LOOP('',(#5218,#5219,#5220,#5221));
#1418=EDGE_LOOP('',(#5222,#5223,#5224,#5225,#5226,#5227));
#1419=EDGE_LOOP('',(#5228));
#1420=EDGE_LOOP('',(#5229,#5230,#5231,#5232,#5233,#5234));
#1421=EDGE_LOOP('',(#5235,#5236,#5237,#5238));
#1422=EDGE_LOOP('',(#5239,#5240,#5241,#5242));
#1777=LINE('',#10836,#2151);
#1778=LINE('',#10838,#2152);
#1779=LINE('',#10840,#2153);
#1780=LINE('',#10841,#2154);
#1781=LINE('',#10844,#2155);
#1782=LINE('',#10846,#2156);
#1783=LINE('',#10847,#2157);
#1784=LINE('',#10850,#2158);
#1785=LINE('',#10852,#2159);
#1786=LINE('',#10853,#2160);
#1787=LINE('',#10856,#2161);
#1788=LINE('',#10858,#2162);
#1789=LINE('',#10859,#2163);
#1790=LINE('',#10862,#2164);
#1791=LINE('',#10864,#2165);
#1792=LINE('',#10865,#2166);
#1793=LINE('',#10867,#2167);
#1794=LINE('',#10868,#2168);
#1795=LINE('',#10876,#2169);
#1796=LINE('',#10878,#2170);
#2151=VECTOR('',#8525,1.);
#2152=VECTOR('',#8526,1.);
#2153=VECTOR('',#8527,1.);
#2154=VECTOR('',#8528,1.);
#2155=VECTOR('',#8531,1.);
#2156=VECTOR('',#8532,1.);
#2157=VECTOR('',#8533,1.);
#2158=VECTOR('',#8536,1.);
#2159=VECTOR('',#8537,1.);
#2160=VECTOR('',#8538,1.);
#2161=VECTOR('',#8541,1.);
#2162=VECTOR('',#8542,1.);
#2163=VECTOR('',#8543,1.);
#2164=VECTOR('',#8546,1.);
#2165=VECTOR('',#8547,1.);
#2166=VECTOR('',#8548,1.);
#2167=VECTOR('',#8551,1.);
#2168=VECTOR('',#8552,1.);
#2169=VECTOR('',#8563,0.185);
#2170=VECTOR('',#8566,0.2);
#2502=CIRCLE('',#6719,0.1954);
#2503=CIRCLE('',#6728,0.17);
#2504=CIRCLE('',#6730,0.1954);
#2984=VERTEX_POINT('',#10831);
#2985=VERTEX_POINT('',#10834);
#2986=VERTEX_POINT('',#10835);
#2987=VERTEX_POINT('',#10837);
#2988=VERTEX_POINT('',#10839);
#2989=VERTEX_POINT('',#10843);
#2990=VERTEX_POINT('',#10845);
#2991=VERTEX_POINT('',#10849);
#2992=VERTEX_POINT('',#10851);
#2993=VERTEX_POINT('',#10855);
#2994=VERTEX_POINT('',#10857);
#2995=VERTEX_POINT('',#10861);
#2996=VERTEX_POINT('',#10863);
#2997=VERTEX_POINT('',#10871);
#2998=VERTEX_POINT('',#10874);
#3724=EDGE_CURVE('',#2984,#2984,#2502,.T.);
#3725=EDGE_CURVE('',#2985,#2986,#1777,.T.);
#3726=EDGE_CURVE('',#2985,#2987,#1778,.T.);
#3727=EDGE_CURVE('',#2987,#2988,#1779,.T.);
#3728=EDGE_CURVE('',#2986,#2988,#1780,.T.);
#3729=EDGE_CURVE('',#2989,#2985,#1781,.T.);
#3730=EDGE_CURVE('',#2989,#2990,#1782,.T.);
#3731=EDGE_CURVE('',#2990,#2987,#1783,.T.);
#3732=EDGE_CURVE('',#2991,#2989,#1784,.T.);
#3733=EDGE_CURVE('',#2991,#2992,#1785,.T.);
#3734=EDGE_CURVE('',#2992,#2990,#1786,.T.);
#3735=EDGE_CURVE('',#2993,#2991,#1787,.T.);
#3736=EDGE_CURVE('',#2993,#2994,#1788,.T.);
#3737=EDGE_CURVE('',#2994,#2992,#1789,.T.);
#3738=EDGE_CURVE('',#2995,#2993,#1790,.T.);
#3739=EDGE_CURVE('',#2995,#2996,#1791,.T.);
#3740=EDGE_CURVE('',#2996,#2994,#1792,.T.);
#3741=EDGE_CURVE('',#2986,#2995,#1793,.T.);
#3742=EDGE_CURVE('',#2988,#2996,#1794,.T.);
#3743=EDGE_CURVE('',#2997,#2997,#2503,.T.);
#3744=EDGE_CURVE('',#2998,#2998,#2504,.T.);
#3745=EDGE_CURVE('',#2998,#2997,#1795,.T.);
#3746=EDGE_CURVE('',#2984,#2998,#1796,.T.);
#5197=ORIENTED_EDGE('',*,*,#3724,.F.);
#5198=ORIENTED_EDGE('',*,*,#3725,.F.);
#5199=ORIENTED_EDGE('',*,*,#3726,.T.);
#5200=ORIENTED_EDGE('',*,*,#3727,.T.);
#5201=ORIENTED_EDGE('',*,*,#3728,.F.);
#5202=ORIENTED_EDGE('',*,*,#3729,.F.);
#5203=ORIENTED_EDGE('',*,*,#3730,.T.);
#5204=ORIENTED_EDGE('',*,*,#3731,.T.);
#5205=ORIENTED_EDGE('',*,*,#3726,.F.);
#5206=ORIENTED_EDGE('',*,*,#3732,.F.);
#5207=ORIENTED_EDGE('',*,*,#3733,.T.);
#5208=ORIENTED_EDGE('',*,*,#3734,.T.);
#5209=ORIENTED_EDGE('',*,*,#3730,.F.);
#5210=ORIENTED_EDGE('',*,*,#3735,.F.);
#5211=ORIENTED_EDGE('',*,*,#3736,.T.);
#5212=ORIENTED_EDGE('',*,*,#3737,.T.);
#5213=ORIENTED_EDGE('',*,*,#3733,.F.);
#5214=ORIENTED_EDGE('',*,*,#3738,.F.);
#5215=ORIENTED_EDGE('',*,*,#3739,.T.);
#5216=ORIENTED_EDGE('',*,*,#3740,.T.);
#5217=ORIENTED_EDGE('',*,*,#3736,.F.);
#5218=ORIENTED_EDGE('',*,*,#3741,.F.);
#5219=ORIENTED_EDGE('',*,*,#3728,.T.);
#5220=ORIENTED_EDGE('',*,*,#3742,.T.);
#5221=ORIENTED_EDGE('',*,*,#3739,.F.);
#5222=ORIENTED_EDGE('',*,*,#3742,.F.);
#5223=ORIENTED_EDGE('',*,*,#3727,.F.);
#5224=ORIENTED_EDGE('',*,*,#3731,.F.);
#5225=ORIENTED_EDGE('',*,*,#3734,.F.);
#5226=ORIENTED_EDGE('',*,*,#3737,.F.);
#5227=ORIENTED_EDGE('',*,*,#3740,.F.);
#5228=ORIENTED_EDGE('',*,*,#3743,.F.);
#5229=ORIENTED_EDGE('',*,*,#3725,.T.);
#5230=ORIENTED_EDGE('',*,*,#3741,.T.);
#5231=ORIENTED_EDGE('',*,*,#3738,.T.);
#5232=ORIENTED_EDGE('',*,*,#3735,.T.);
#5233=ORIENTED_EDGE('',*,*,#3732,.T.);
#5234=ORIENTED_EDGE('',*,*,#3729,.T.);
#5235=ORIENTED_EDGE('',*,*,#3744,.F.);
#5236=ORIENTED_EDGE('',*,*,#3745,.T.);
#5237=ORIENTED_EDGE('',*,*,#3743,.T.);
#5238=ORIENTED_EDGE('',*,*,#3745,.F.);
#5239=ORIENTED_EDGE('',*,*,#3724,.T.);
#5240=ORIENTED_EDGE('',*,*,#3746,.T.);
#5241=ORIENTED_EDGE('',*,*,#3744,.T.);
#5242=ORIENTED_EDGE('',*,*,#3746,.F.);
#5365=CYLINDRICAL_SURFACE('',#6731,0.1954);
#5688=ADVANCED_FACE('',(#974),#643,.F.);
#5689=ADVANCED_FACE('',(#975),#644,.F.);
#5690=ADVANCED_FACE('',(#976),#645,.F.);
#5691=ADVANCED_FACE('',(#977),#646,.F.);
#5692=ADVANCED_FACE('',(#978),#647,.F.);
#5693=ADVANCED_FACE('',(#979),#648,.F.);
#5694=ADVANCED_FACE('',(#980),#649,.F.);
#5695=ADVANCED_FACE('',(#981),#650,.F.);
#5696=ADVANCED_FACE('',(#982,#471),#651,.T.);
#5697=ADVANCED_FACE('',(#983),#210,.T.);
#5698=ADVANCED_FACE('',(#984),#5365,.T.);
#5733=CLOSED_SHELL('',(#5688,#5689,#5690,#5691,#5692,#5693,#5694,#5695,
#5696,#5697,#5698));
#6717=AXIS2_PLACEMENT_3D('',#10829,#8517,#8518);
#6718=AXIS2_PLACEMENT_3D('',#10830,#8519,#8520);
#6719=AXIS2_PLACEMENT_3D('',#10832,#8521,#8522);
#6720=AXIS2_PLACEMENT_3D('',#10833,#8523,#8524);
#6721=AXIS2_PLACEMENT_3D('',#10842,#8529,#8530);
#6722=AXIS2_PLACEMENT_3D('',#10848,#8534,#8535);
#6723=AXIS2_PLACEMENT_3D('',#10854,#8539,#8540);
#6724=AXIS2_PLACEMENT_3D('',#10860,#8544,#8545);
#6725=AXIS2_PLACEMENT_3D('',#10866,#8549,#8550);
#6726=AXIS2_PLACEMENT_3D('',#10869,#8553,#8554);
#6727=AXIS2_PLACEMENT_3D('',#10870,#8555,#8556);
#6728=AXIS2_PLACEMENT_3D('',#10872,#8557,#8558);
#6729=AXIS2_PLACEMENT_3D('',#10873,#8559,#8560);
#6730=AXIS2_PLACEMENT_3D('',#10875,#8561,#8562);
#6731=AXIS2_PLACEMENT_3D('',#10877,#8564,#8565);
#8517=DIRECTION('axis',(0.,0.,1.));
#8518=DIRECTION('refdir',(1.,0.,0.));
#8519=DIRECTION('center_axis',(0.,1.,0.));
#8520=DIRECTION('ref_axis',(1.,0.,0.));
#8521=DIRECTION('center_axis',(0.,1.,0.));
#8522=DIRECTION('ref_axis',(1.,0.,0.));
#8523=DIRECTION('center_axis',(0.866025403784439,0.,-0.5));
#8524=DIRECTION('ref_axis',(0.5,0.,0.866025403784439));
#8525=DIRECTION('',(0.5,0.,0.866025403784439));
#8526=DIRECTION('',(0.,-1.,0.));
#8527=DIRECTION('',(0.5,0.,0.866025403784439));
#8528=DIRECTION('',(0.,-1.,0.));
#8529=DIRECTION('center_axis',(1.20185167898973E-16,0.,-1.));
#8530=DIRECTION('ref_axis',(1.,0.,1.20185167898973E-16));
#8531=DIRECTION('',(1.,0.,1.20185167898973E-16));
#8532=DIRECTION('',(0.,-1.,0.));
#8533=DIRECTION('',(1.,0.,1.20185167898973E-16));
#8534=DIRECTION('center_axis',(-0.866025403784439,0.,-0.5));
#8535=DIRECTION('ref_axis',(0.5,0.,-0.866025403784439));
#8536=DIRECTION('',(0.5,0.,-0.866025403784439));
#8537=DIRECTION('',(0.,-1.,0.));
#8538=DIRECTION('',(0.5,0.,-0.866025403784439));
#8539=DIRECTION('center_axis',(-0.866025403784439,0.,0.5));
#8540=DIRECTION('ref_axis',(-0.5,0.,-0.866025403784439));
#8541=DIRECTION('',(-0.5,0.,-0.866025403784439));
#8542=DIRECTION('',(0.,-1.,0.));
#8543=DIRECTION('',(-0.5,0.,-0.866025403784439));
#8544=DIRECTION('center_axis',(-2.40370335797945E-16,0.,1.));
#8545=DIRECTION('ref_axis',(-1.,0.,-2.40370335797945E-16));
#8546=DIRECTION('',(-1.,0.,-2.40370335797945E-16));
#8547=DIRECTION('',(0.,-1.,0.));
#8548=DIRECTION('',(-1.,0.,-2.40370335797945E-16));
#8549=DIRECTION('center_axis',(0.866025403784439,0.,0.5));
#8550=DIRECTION('ref_axis',(-0.5,0.,0.866025403784439));
#8551=DIRECTION('',(-0.5,0.,0.866025403784439));
#8552=DIRECTION('',(-0.5,0.,0.866025403784439));
#8553=DIRECTION('center_axis',(0.,-1.,0.));
#8554=DIRECTION('ref_axis',(0.,0.,-1.));
#8555=DIRECTION('center_axis',(0.,1.,0.));
#8556=DIRECTION('ref_axis',(0.,0.,1.));
#8557=DIRECTION('center_axis',(0.,-1.,0.));
#8558=DIRECTION('ref_axis',(1.,0.,0.));
#8559=DIRECTION('center_axis',(0.,-1.,0.));
#8560=DIRECTION('ref_axis',(1.,0.,0.));
#8561=DIRECTION('center_axis',(0.,-1.,0.));
#8562=DIRECTION('ref_axis',(1.,0.,0.));
#8563=DIRECTION('',(0.707106781186548,0.707106781186547,8.65956056235494E-17));
#8564=DIRECTION('center_axis',(0.,-1.,0.));
#8565=DIRECTION('ref_axis',(1.,0.,0.));
#8566=DIRECTION('',(0.,1.,0.));
#10829=CARTESIAN_POINT('',(0.,0.,0.));
#10830=CARTESIAN_POINT('Origin',(0.,-0.4,0.));
#10831=CARTESIAN_POINT('',(-0.1954,-0.4,2.39295984553393E-17));
#10832=CARTESIAN_POINT('Origin',(0.,-0.4,0.));
#10833=CARTESIAN_POINT('Origin',(0.0577350269189626,0.,-0.1));
#10834=CARTESIAN_POINT('',(0.0577350269189626,0.,-0.1));
#10835=CARTESIAN_POINT('',(0.115470053837925,0.,0.));
#10836=CARTESIAN_POINT('',(0.0934187836487032,0.,-0.0381939203391614));
#10837=CARTESIAN_POINT('',(0.0577350269189626,-0.2,-0.1));
#10838=CARTESIAN_POINT('',(0.0577350269189626,0.,-0.1));
#10839=CARTESIAN_POINT('',(0.115470053837925,-0.2,0.));
#10840=CARTESIAN_POINT('',(0.115470053837925,-0.2,0.));
#10841=CARTESIAN_POINT('',(0.115470053837925,0.,0.));
#10842=CARTESIAN_POINT('Origin',(-0.0577350269189626,0.,-0.1));
#10843=CARTESIAN_POINT('',(-0.0577350269189626,0.,-0.1));
#10844=CARTESIAN_POINT('',(0.0561324865405187,0.,-0.1));
#10845=CARTESIAN_POINT('',(-0.0577350269189626,-0.2,-0.1));
#10846=CARTESIAN_POINT('',(-0.0577350269189626,0.,-0.1));
#10847=CARTESIAN_POINT('',(0.0577350269189626,-0.2,-0.1));
#10848=CARTESIAN_POINT('Origin',(-0.115470053837925,0.,-1.38777878078145E-17));
#10849=CARTESIAN_POINT('',(-0.115470053837925,0.,-1.41410031829988E-17));
#10850=CARTESIAN_POINT('',(-0.0797862971081845,0.,-0.0618060796608387));
#10851=CARTESIAN_POINT('',(-0.115470053837925,-0.2,-1.38777878078145E-17));
#10852=CARTESIAN_POINT('',(-0.115470053837925,0.,-1.41410031829988E-17));
#10853=CARTESIAN_POINT('',(-0.0577350269189626,-0.2,-0.1));
#10854=CARTESIAN_POINT('Origin',(-0.0577350269189626,0.,0.1));
#10855=CARTESIAN_POINT('',(-0.0577350269189626,0.,0.1));
#10856=CARTESIAN_POINT('',(-0.0509187836487033,0.,0.111806079660839));
#10857=CARTESIAN_POINT('',(-0.0577350269189626,-0.2,0.1));
#10858=CARTESIAN_POINT('',(-0.0577350269189626,0.,0.1));
#10859=CARTESIAN_POINT('',(-0.115470053837925,-0.2,-1.41410031829988E-17));
#10860=CARTESIAN_POINT('Origin',(0.0577350269189626,0.,0.1));
#10861=CARTESIAN_POINT('',(0.0577350269189626,0.,0.1));
#10862=CARTESIAN_POINT('',(0.113867513459481,0.,0.1));
#10863=CARTESIAN_POINT('',(0.0577350269189626,-0.2,0.1));
#10864=CARTESIAN_POINT('',(0.0577350269189626,0.,0.1));
#10865=CARTESIAN_POINT('',(-0.0577350269189626,-0.2,0.1));
#10866=CARTESIAN_POINT('Origin',(0.115470053837925,0.,0.));
#10867=CARTESIAN_POINT('',(0.122286297108185,0.,-0.0118060796608386));
#10868=CARTESIAN_POINT('',(0.0577350269189626,-0.2,0.1));
#10869=CARTESIAN_POINT('Origin',(0.,-0.2,0.));
#10870=CARTESIAN_POINT('Origin',(0.17,0.,0.));
#10871=CARTESIAN_POINT('',(-0.17,-8.67361737988404E-18,-2.0818995585505E-17));
#10872=CARTESIAN_POINT('Origin',(0.,0.,0.));
#10873=CARTESIAN_POINT('Origin',(0.,-0.015,0.));
#10874=CARTESIAN_POINT('',(-0.1954,-0.0254,-2.39295984553393E-17));
#10875=CARTESIAN_POINT('Origin',(0.,-0.0254,0.));
#10876=CARTESIAN_POINT('',(-0.185,-0.015,-2.2655965784226E-17));
#10877=CARTESIAN_POINT('Origin',(0.,-0.2775,0.));
#10878=CARTESIAN_POINT('',(-0.1954,-0.2775,-2.39295984553393E-17));
#10925=UNCERTAINTY_MEASURE_WITH_UNIT(LENGTH_MEASURE(0.001),#10958,
'DISTANCE_ACCURACY_VALUE',
'Maximum model space distance between geometric entities at asserted c
onnectivities');
#10926=UNCERTAINTY_MEASURE_WITH_UNIT(LENGTH_MEASURE(0.001),#10958,
'DISTANCE_ACCURACY_VALUE',
'Maximum model space distance between geometric entities at asserted c
onnectivities');
#10956=(
GEOMETRIC_REPRESENTATION_CONTEXT(3)
GLOBAL_UNCERTAINTY_ASSIGNED_CONTEXT((#10925))
GLOBAL_UNIT_ASSIGNED_CONTEXT((#10958,#10960,#10961))
REPRESENTATION_CONTEXT('','3D')
);
#10957=(
GEOMETRIC_REPRESENTATION_CONTEXT(3)
GLOBAL_UNCERTAINTY_ASSIGNED_CONTEXT((#10926))
GLOBAL_UNIT_ASSIGNED_CONTEXT((#10958,#10960,#10961))
REPRESENTATION_CONTEXT('','3D')
);
#10958=(
LENGTH_UNIT()
NAMED_UNIT(*)
SI_UNIT(.CENTI.,.METRE.)
);
#10960=(
NAMED_UNIT(*)
PLANE_ANGLE_UNIT()
SI_UNIT($,.RADIAN.)
);
#10961=(
NAMED_UNIT(*)
SI_UNIT($,.STERADIAN.)
SOLID_ANGLE_UNIT()
);
#10991=SHAPE_DEFINITION_REPRESENTATION(#11046,#11093);
#11046=PRODUCT_DEFINITION_SHAPE('',$,#11124);
#11093=SHAPE_REPRESENTATION('',(#6717),#10956);
#11094=PRODUCT_DEFINITION_CONTEXT('part definition',#11186,'design');
#11124=PRODUCT_DEFINITION('M4x4 collar screw','M4x4 collar screw',#11154,
#11094);
#11154=PRODUCT_DEFINITION_FORMATION('',$,#11217);
#11186=APPLICATION_CONTEXT(
'Core Data for Automotive Mechanical Design Process');
#11187=PRODUCT_CONTEXT('part definition',#11186,'mechanical');
#11217=PRODUCT('M4x4 collar screw','M4x4 collar screw',
'M4x4 collar screw',(#11187));
#11288=COLOUR_RGB('Black',0.12,0.14,0.17);
#11289=FILL_AREA_STYLE_COLOUR('',#11288);
#11290=FILL_AREA_STYLE('',(#11289));
#11291=SURFACE_STYLE_FILL_AREA(#11290);
#11292=SURFACE_SIDE_STYLE('',(#11291));
#11293=SURFACE_STYLE_USAGE(.BOTH.,#11292);
#11294=PRESENTATION_STYLE_ASSIGNMENT((#11293));
ENDSEC;
END-ISO-10303-21;
